ISO-10303-21;
HEADER;
/* Generated by software containing ST-Developer
 * from STEP Tools, Inc. (www.steptools.com) 
 */

FILE_DESCRIPTION(
/* description */ ('PAT-122'),
/* implementation_level */ '2;1');

FILE_NAME(
/* name */ 'M5x14 Cap Screw.step',
/* time_stamp */ '2026-10-29T20:20:12-07:00',
/* author */ (''),
/* organization */ (''),
/* preprocessor_version */ 'ST-DEVELOPER v20.2',
/* originating_system */ 'Autodesk Translation Framework v15.17.0.0',
/* authorisation */ '');

FILE_SCHEMA (('AUTOMOTIVE_DESIGN { 1 0 10303 214 3 1 1 }'));
ENDSEC;

DATA;
#10=MECHANICAL_DESIGN_GEOMETRIC_PRESENTATION_REPRESENTATION('',(#510),#10019);
#409=CONICAL_SURFACE('',#6281,0.4,0.785398163397448);
#410=CONICAL_SURFACE('',#6285,0.41,0.785398163397448);
#411=CONICAL_SURFACE('',#6289,0.26,0.463647609000806);
#419=ORIENTED_CLOSED_SHELL('',*,#5634,.F.);
#423=BREP_WITH_VOIDS('Body1',#5635,(#419));
#466=SHAPE_REPRESENTATION_RELATIONSHIP('SRR','None',#10187,#488);
#488=ADVANCED_BREP_SHAPE_REPRESENTATION('',(#423),#10016);
#510=STYLED_ITEM('',(#10355),#423);
#605=FACE_BOUND('',#1459,.T.);
#801=PLANE('',#6269);
#802=PLANE('',#6270);
#803=PLANE('',#6271);
#804=PLANE('',#6272);
#805=PLANE('',#6273);
#806=PLANE('',#6274);
#807=PLANE('',#6275);
#808=PLANE('',#6276);
#809=PLANE('',#6277);
#810=PLANE('',#6279);
#811=PLANE('',#6287);
#1079=FACE_OUTER_BOUND('',#1445,.T.);
#1080=FACE_OUTER_BOUND('',#1446,.T.);
#1081=FACE_OUTER_BOUND('',#1447,.T.);
#1082=FACE_OUTER_BOUND('',#1448,.T.);
#1083=FACE_OUTER_BOUND('',#1449,.T.);
#1084=FACE_OUTER_BOUND('',#1450,.T.);
#1085=FACE_OUTER_BOUND('',#1451,.T.);
#1086=FACE_OUTER_BOUND('',#1452,.T.);
#1087=FACE_OUTER_BOUND('',#1453,.T.);
#1088=FACE_OUTER_BOUND('',#1454,.T.);
#1089=FACE_OUTER_BOUND('',#1455,.T.);
#1090=FACE_OUTER_BOUND('',#1456,.T.);
#1091=FACE_OUTER_BOUND('',#1457,.T.);
#1092=FACE_OUTER_BOUND('',#1458,.T.);
#1093=FACE_OUTER_BOUND('',#1460,.T.);
#1094=FACE_OUTER_BOUND('',#1461,.T.);
#1445=EDGE_LOOP('',(#5121,#5122,#5123,#5124));
#1446=EDGE_LOOP('',(#5125,#5126,#5127,#5128));
#1447=EDGE_LOOP('',(#5129,#5130,#5131,#5132));
#1448=EDGE_LOOP('',(#5133,#5134,#5135,#5136));
#1449=EDGE_LOOP('',(#5137,#5138,#5139,#5140));
#1450=EDGE_LOOP('',(#5141,#5142,#5143,#5144));
#1451=EDGE_LOOP('',(#5145,#5146,#5147,#5148,#5149,#5150));
#1452=EDGE_LOOP('',(#5151,#5152,#5153,#5154,#5155,#5156));
#1453=EDGE_LOOP('',(#5157));
#1454=EDGE_LOOP('',(#5158));
#1455=EDGE_LOOP('',(#5159,#5160,#5161,#5162));
#1456=EDGE_LOOP('',(#5163,#5164,#5165,#5166));
#1457=EDGE_LOOP('',(#5167,#5168,#5169,#5170));
#1458=EDGE_LOOP('',(#5171));
#1459=EDGE_LOOP('',(#5172));
#1460=EDGE_LOOP('',(#5173,#5174,#5175,#5176));
#1461=EDGE_LOOP('',(#5177,#5178,#5179,#5180));
#1981=LINE('',#9724,#2525);
#1982=LINE('',#9726,#2526);
#1983=LINE('',#9728,#2527);
#1984=LINE('',#9729,#2528);
#1985=LINE('',#9732,#2529);
#1986=LINE('',#9734,#2530);
#1987=LINE('',#9735,#2531);
#1988=LINE('',#9738,#2532);
#1989=LINE('',#9740,#2533);
#1990=LINE('',#9741,#2534);
#1991=LINE('',#9744,#2535);
#1992=LINE('',#9746,#2536);
#1993=LINE('',#9747,#2537);
#1994=LINE('',#9750,#2538);
#1995=LINE('',#9752,#2539);
#1996=LINE('',#9753,#2540);
#1997=LINE('',#9755,#2541);
#1998=LINE('',#9756,#2542);
#1999=LINE('',#9768,#2543);
#2000=LINE('',#9772,#2544);
#2001=LINE('',#9776,#2545);
#2002=LINE('',#9783,#2546);
#2003=LINE('',#9785,#2547);
#2525=VECTOR('',#7696,1.);
#2526=VECTOR('',#7697,1.);
#2527=VECTOR('',#7698,1.);
#2528=VECTOR('',#7699,1.);
#2529=VECTOR('',#7702,1.);
#2530=VECTOR('',#7703,1.);
#2531=VECTOR('',#7704,1.);
#2532=VECTOR('',#7707,1.);
#2533=VECTOR('',#7708,1.);
#2534=VECTOR('',#7709,1.);
#2535=VECTOR('',#7712,1.);
#2536=VECTOR('',#7713,1.);
#2537=VECTOR('',#7714,1.);
#2538=VECTOR('',#7717,1.);
#2539=VECTOR('',#7718,1.);
#2540=VECTOR('',#7719,1.);
#2541=VECTOR('',#7722,1.);
#2542=VECTOR('',#7723,1.);
#2543=VECTOR('',#7740,0.4);
#2544=VECTOR('',#7745,0.425);
#2545=VECTOR('',#7750,0.41);
#2546=VECTOR('',#7759,0.26);
#2547=VECTOR('',#7762,0.25);
#2685=CIRCLE('',#6278,0.24505);
#2686=CIRCLE('',#6280,0.375);
#2687=CIRCLE('',#6282,0.425);
#2688=CIRCLE('',#6284,0.425);
#2689=CIRCLE('',#6286,0.395);
#2690=CIRCLE('',#6288,0.27);
#2691=CIRCLE('',#6290,0.24505);
#3123=VERTEX_POINT('',#9722);
#3124=VERTEX_POINT('',#9723);
#3125=VERTEX_POINT('',#9725);
#3126=VERTEX_POINT('',#9727);
#3127=VERTEX_POINT('',#9731);
#3128=VERTEX_POINT('',#9733);
#3129=VERTEX_POINT('',#9737);
#3130=VERTEX_POINT('',#9739);
#3131=VERTEX_POINT('',#9743);
#3132=VERTEX_POINT('',#9745);
#3133=VERTEX_POINT('',#9749);
#3134=VERTEX_POINT('',#9751);
#3135=VERTEX_POINT('',#9760);
#3136=VERTEX_POINT('',#9763);
#3137=VERTEX_POINT('',#9766);
#3138=VERTEX_POINT('',#9770);
#3139=VERTEX_POINT('',#9774);
#3140=VERTEX_POINT('',#9778);
#3141=VERTEX_POINT('',#9781);
#3795=EDGE_CURVE('',#3123,#3124,#1981,.T.);
#3796=EDGE_CURVE('',#3124,#3125,#1982,.T.);
#3797=EDGE_CURVE('',#3125,#3126,#1983,.T.);
#3798=EDGE_CURVE('',#3123,#3126,#1984,.T.);
#3799=EDGE_CURVE('',#3124,#3127,#1985,.T.);
#3800=EDGE_CURVE('',#3127,#3128,#1986,.T.);
#3801=EDGE_CURVE('',#3128,#3125,#1987,.T.);
#3802=EDGE_CURVE('',#3127,#3129,#1988,.T.);
#3803=EDGE_CURVE('',#3129,#3130,#1989,.T.);
#3804=EDGE_CURVE('',#3130,#3128,#1990,.T.);
#3805=EDGE_CURVE('',#3129,#3131,#1991,.T.);
#3806=EDGE_CURVE('',#3131,#3132,#1992,.T.);
#3807=EDGE_CURVE('',#3132,#3130,#1993,.T.);
#3808=EDGE_CURVE('',#3131,#3133,#1994,.T.);
#3809=EDGE_CURVE('',#3133,#3134,#1995,.T.);
#3810=EDGE_CURVE('',#3134,#3132,#1996,.T.);
#3811=EDGE_CURVE('',#3133,#3123,#1997,.T.);
#3812=EDGE_CURVE('',#3126,#3134,#1998,.T.);
#3813=EDGE_CURVE('',#3135,#3135,#2685,.T.);
#3814=EDGE_CURVE('',#3136,#3136,#2686,.T.);
#3815=EDGE_CURVE('',#3137,#3137,#2687,.T.);
#3816=EDGE_CURVE('',#3137,#3136,#1999,.T.);
#3817=EDGE_CURVE('',#3138,#3138,#2688,.T.);
#3818=EDGE_CURVE('',#3138,#3137,#2000,.T.);
#3819=EDGE_CURVE('',#3139,#3139,#2689,.T.);
#3820=EDGE_CURVE('',#3139,#3138,#2001,.T.);
#3821=EDGE_CURVE('',#3140,#3140,#2690,.T.);
#3822=EDGE_CURVE('',#3141,#3141,#2691,.F.);
#3823=EDGE_CURVE('',#3141,#3140,#2002,.T.);
#3824=EDGE_CURVE('',#3135,#3141,#2003,.T.);
#5121=ORIENTED_EDGE('',*,*,#3795,.T.);
#5122=ORIENTED_EDGE('',*,*,#3796,.T.);
#5123=ORIENTED_EDGE('',*,*,#3797,.T.);
#5124=ORIENTED_EDGE('',*,*,#3798,.F.);
#5125=ORIENTED_EDGE('',*,*,#3799,.T.);
#5126=ORIENTED_EDGE('',*,*,#3800,.T.);
#5127=ORIENTED_EDGE('',*,*,#3801,.T.);
#5128=ORIENTED_EDGE('',*,*,#3796,.F.);
#5129=ORIENTED_EDGE('',*,*,#3802,.T.);
#5130=ORIENTED_EDGE('',*,*,#3803,.T.);
#5131=ORIENTED_EDGE('',*,*,#3804,.T.);
#5132=ORIENTED_EDGE('',*,*,#3800,.F.);
#5133=ORIENTED_EDGE('',*,*,#3805,.T.);
#5134=ORIENTED_EDGE('',*,*,#3806,.T.);
#5135=ORIENTED_EDGE('',*,*,#3807,.T.);
#5136=ORIENTED_EDGE('',*,*,#3803,.F.);
#5137=ORIENTED_EDGE('',*,*,#3808,.T.);
#5138=ORIENTED_EDGE('',*,*,#3809,.T.);
#5139=ORIENTED_EDGE('',*,*,#3810,.T.);
#5140=ORIENTED_EDGE('',*,*,#3806,.F.);
#5141=ORIENTED_EDGE('',*,*,#3811,.T.);
#5142=ORIENTED_EDGE('',*,*,#3798,.T.);
#5143=ORIENTED_EDGE('',*,*,#3812,.T.);
#5144=ORIENTED_EDGE('',*,*,#3809,.F.);
#5145=ORIENTED_EDGE('',*,*,#3811,.F.);
#5146=ORIENTED_EDGE('',*,*,#3808,.F.);
#5147=ORIENTED_EDGE('',*,*,#3805,.F.);
#5148=ORIENTED_EDGE('',*,*,#3802,.F.);
#5149=ORIENTED_EDGE('',*,*,#3799,.F.);
#5150=ORIENTED_EDGE('',*,*,#3795,.F.);
#5151=ORIENTED_EDGE('',*,*,#3812,.F.);
#5152=ORIENTED_EDGE('',*,*,#3797,.F.);
#5153=ORIENTED_EDGE('',*,*,#3801,.F.);
#5154=ORIENTED_EDGE('',*,*,#3804,.F.);
#5155=ORIENTED_EDGE('',*,*,#3807,.F.);
#5156=ORIENTED_EDGE('',*,*,#3810,.F.);
#5157=ORIENTED_EDGE('',*,*,#3813,.F.);
#5158=ORIENTED_EDGE('',*,*,#3814,.F.);
#5159=ORIENTED_EDGE('',*,*,#3815,.F.);
#5160=ORIENTED_EDGE('',*,*,#3816,.T.);
#5161=ORIENTED_EDGE('',*,*,#3814,.T.);
#5162=ORIENTED_EDGE('',*,*,#3816,.F.);
#5163=ORIENTED_EDGE('',*,*,#3817,.F.);
#5164=ORIENTED_EDGE('',*,*,#3818,.T.);
#5165=ORIENTED_EDGE('',*,*,#3815,.T.);
#5166=ORIENTED_EDGE('',*,*,#3818,.F.);
#5167=ORIENTED_EDGE('',*,*,#3819,.F.);
#5168=ORIENTED_EDGE('',*,*,#3820,.T.);
#5169=ORIENTED_EDGE('',*,*,#3817,.T.);
#5170=ORIENTED_EDGE('',*,*,#3820,.F.);
#5171=ORIENTED_EDGE('',*,*,#3819,.T.);
#5172=ORIENTED_EDGE('',*,*,#3821,.F.);
#5173=ORIENTED_EDGE('',*,*,#3822,.F.);
#5174=ORIENTED_EDGE('',*,*,#3823,.T.);
#5175=ORIENTED_EDGE('',*,*,#3821,.T.);
#5176=ORIENTED_EDGE('',*,*,#3823,.F.);
#5177=ORIENTED_EDGE('',*,*,#3813,.T.);
#5178=ORIENTED_EDGE('',*,*,#3824,.T.);
#5179=ORIENTED_EDGE('',*,*,#3822,.T.);
#5180=ORIENTED_EDGE('',*,*,#3824,.F.);
#5315=CYLINDRICAL_SURFACE('',#6283,0.425);
#5316=CYLINDRICAL_SURFACE('',#6291,0.24505);
#5575=ADVANCED_FACE('',(#1079),#801,.F.);
#5576=ADVANCED_FACE('',(#1080),#802,.F.);
#5577=ADVANCED_FACE('',(#1081),#803,.F.);
#5578=ADVANCED_FACE('',(#1082),#804,.F.);
#5579=ADVANCED_FACE('',(#1083),#805,.F.);
#5580=ADVANCED_FACE('',(#1084),#806,.F.);
#5581=ADVANCED_FACE('',(#1085),#807,.F.);
#5582=ADVANCED_FACE('',(#1086),#808,.F.);
#5583=ADVANCED_FACE('',(#1087),#809,.F.);
#5584=ADVANCED_FACE('',(#1088),#810,.T.);
#5585=ADVANCED_FACE('',(#1089),#409,.T.);
#5586=ADVANCED_FACE('',(#1090),#5315,.T.);
#5587=ADVANCED_FACE('',(#1091),#410,.T.);
#5588=ADVANCED_FACE('',(#1092,#605),#811,.T.);
#5589=ADVANCED_FACE('',(#1093),#411,.T.);
#5590=ADVANCED_FACE('',(#1094),#5316,.T.);
#5634=CLOSED_SHELL('',(#5575,#5576,#5577,#5578,#5579,#5580,#5581,#5582));
#5635=CLOSED_SHELL('',(#5583,#5584,#5585,#5586,#5587,#5588,#5589,#5590));
#6268=AXIS2_PLACEMENT_3D('',#9720,#7692,#7693);
#6269=AXIS2_PLACEMENT_3D('',#9721,#7694,#7695);
#6270=AXIS2_PLACEMENT_3D('',#9730,#7700,#7701);
#6271=AXIS2_PLACEMENT_3D('',#9736,#7705,#7706);
#6272=AXIS2_PLACEMENT_3D('',#9742,#7710,#7711);
#6273=AXIS2_PLACEMENT_3D('',#9748,#7715,#7716);
#6274=AXIS2_PLACEMENT_3D('',#9754,#7720,#7721);
#6275=AXIS2_PLACEMENT_3D('',#9757,#7724,#7725);
#6276=AXIS2_PLACEMENT_3D('',#9758,#7726,#7727);
#6277=AXIS2_PLACEMENT_3D('',#9759,#7728,#7729);
#6278=AXIS2_PLACEMENT_3D('',#9761,#7730,#7731);
#6279=AXIS2_PLACEMENT_3D('',#9762,#7732,#7733);
#6280=AXIS2_PLACEMENT_3D('',#9764,#7734,#7735);
#6281=AXIS2_PLACEMENT_3D('',#9765,#7736,#7737);
#6282=AXIS2_PLACEMENT_3D('',#9767,#7738,#7739);
#6283=AXIS2_PLACEMENT_3D('',#9769,#7741,#7742);
#6284=AXIS2_PLACEMENT_3D('',#9771,#7743,#7744);
#6285=AXIS2_PLACEMENT_3D('',#9773,#7746,#7747);
#6286=AXIS2_PLACEMENT_3D('',#9775,#7748,#7749);
#6287=AXIS2_PLACEMENT_3D('',#9777,#7751,#7752);
#6288=AXIS2_PLACEMENT_3D('',#9779,#7753,#7754);
#6289=AXIS2_PLACEMENT_3D('',#9780,#7755,#7756);
#6290=AXIS2_PLACEMENT_3D('',#9782,#7757,#7758);
#6291=AXIS2_PLACEMENT_3D('',#9784,#7760,#7761);
#7692=DIRECTION('axis',(0.,0.,1.));
#7693=DIRECTION('refdir',(1.,0.,0.));
#7694=DIRECTION('center_axis',(0.866025403784439,0.,-0.5));
#7695=DIRECTION('ref_axis',(0.5,0.,0.866025403784439));
#7696=DIRECTION('',(-0.5,0.,-0.866025403784439));
#7697=DIRECTION('',(0.,-1.,0.));
#7698=DIRECTION('',(0.5,0.,0.866025403784439));
#7699=DIRECTION('',(0.,-1.,0.));
#7700=DIRECTION('center_axis',(1.20185167898973E-16,0.,-1.));
#7701=DIRECTION('ref_axis',(1.,0.,1.20185167898973E-16));
#7702=DIRECTION('',(-1.,0.,-1.20185167898973E-16));
#7703=DIRECTION('',(0.,-1.,0.));
#7704=DIRECTION('',(1.,0.,1.20185167898973E-16));
#7705=DIRECTION('center_axis',(-0.866025403784439,0.,-0.5));
#7706=DIRECTION('ref_axis',(0.5,0.,-0.866025403784439));
#7707=DIRECTION('',(-0.5,0.,0.866025403784439));
#7708=DIRECTION('',(0.,-1.,0.));
#7709=DIRECTION('',(0.5,0.,-0.866025403784439));
#7710=DIRECTION('center_axis',(-0.866025403784439,0.,0.5));
#7711=DIRECTION('ref_axis',(-0.5,0.,-0.866025403784439));
#7712=DIRECTION('',(0.5,0.,0.866025403784439));
#7713=DIRECTION('',(0.,-1.,0.));
#7714=DIRECTION('',(-0.5,0.,-0.866025403784439));
#7715=DIRECTION('center_axis',(-2.40370335797945E-16,0.,1.));
#7716=DIRECTION('ref_axis',(-1.,0.,-2.40370335797945E-16));
#7717=DIRECTION('',(1.,0.,2.40370335797945E-16));
#7718=DIRECTION('',(0.,-1.,0.));
#7719=DIRECTION('',(-1.,0.,-2.40370335797945E-16));
#7720=DIRECTION('center_axis',(0.866025403784439,0.,0.5));
#7721=DIRECTION('ref_axis',(-0.5,0.,0.866025403784439));
#7722=DIRECTION('',(0.5,0.,-0.866025403784439));
#7723=DIRECTION('',(-0.5,0.,0.866025403784439));
#7724=DIRECTION('center_axis',(0.,1.,0.));
#7725=DIRECTION('ref_axis',(1.,0.,0.));
#7726=DIRECTION('center_axis',(0.,-1.,0.));
#7727=DIRECTION('ref_axis',(0.,0.,-1.));
#7728=DIRECTION('center_axis',(0.,1.,0.));
#7729=DIRECTION('ref_axis',(1.,0.,0.));
#7730=DIRECTION('center_axis',(0.,1.,0.));
#7731=DIRECTION('ref_axis',(1.,0.,0.));
#7732=DIRECTION('center_axis',(0.,1.,0.));
#7733=DIRECTION('ref_axis',(0.,0.,1.));
#7734=DIRECTION('center_axis',(0.,-1.,0.));
#7735=DIRECTION('ref_axis',(1.,0.,0.));
#7736=DIRECTION('center_axis',(0.,-1.,0.));
#7737=DIRECTION('ref_axis',(1.,0.,0.));
#7738=DIRECTION('center_axis',(0.,-1.,0.));
#7739=DIRECTION('ref_axis',(1.,0.,0.));
#7740=DIRECTION('',(0.707106781186548,0.707106781186547,8.65956056235493E-17));
#7741=DIRECTION('center_axis',(0.,-1.,0.));
#7742=DIRECTION('ref_axis',(1.,0.,0.));
#7743=DIRECTION('center_axis',(0.,-1.,0.));
#7744=DIRECTION('ref_axis',(1.,0.,0.));
#7745=DIRECTION('',(0.,1.,0.));
#7746=DIRECTION('center_axis',(0.,1.,0.));
#7747=DIRECTION('ref_axis',(1.,0.,0.));
#7748=DIRECTION('center_axis',(0.,-1.,0.));
#7749=DIRECTION('ref_axis',(1.,0.,0.));
#7750=DIRECTION('',(-0.707106781186547,0.707106781186548,-8.65956056235493E-17));
#7751=DIRECTION('center_axis',(0.,-1.,0.));
#7752=DIRECTION('ref_axis',(0.,0.,-1.));
#7753=DIRECTION('center_axis',(0.,-1.,0.));
#7754=DIRECTION('ref_axis',(1.,0.,0.));
#7755=DIRECTION('center_axis',(0.,1.,0.));
#7756=DIRECTION('ref_axis',(1.,0.,0.));
#7757=DIRECTION('center_axis',(0.,1.,0.));
#7758=DIRECTION('ref_axis',(1.,0.,0.));
#7759=DIRECTION('',(-0.447213595499958,0.894427190999916,-5.47678698264203E-17));
#7760=DIRECTION('center_axis',(0.,-1.,0.));
#7761=DIRECTION('ref_axis',(1.,0.,0.));
#7762=DIRECTION('',(0.,1.,0.));
#9720=CARTESIAN_POINT('',(0.,0.,0.));
#9721=CARTESIAN_POINT('Origin',(0.115470053837925,-0.5,-0.2));
#9722=CARTESIAN_POINT('',(0.23094010767585,-0.5,0.));
#9723=CARTESIAN_POINT('',(0.115470053837925,-0.5,-0.2));
#9724=CARTESIAN_POINT('',(0.23094010767585,-0.5,0.));
#9725=CARTESIAN_POINT('',(0.115470053837925,-0.8,-0.2));
#9726=CARTESIAN_POINT('',(0.115470053837925,-0.5,-0.2));
#9727=CARTESIAN_POINT('',(0.23094010767585,-0.8,0.));
#9728=CARTESIAN_POINT('',(0.23094010767585,-0.8,0.));
#9729=CARTESIAN_POINT('',(0.23094010767585,-0.5,0.));
#9730=CARTESIAN_POINT('Origin',(-0.115470053837925,-0.5,-0.2));
#9731=CARTESIAN_POINT('',(-0.115470053837925,-0.5,-0.2));
#9732=CARTESIAN_POINT('',(0.115470053837925,-0.5,-0.2));
#9733=CARTESIAN_POINT('',(-0.115470053837925,-0.8,-0.2));
#9734=CARTESIAN_POINT('',(-0.115470053837925,-0.5,-0.2));
#9735=CARTESIAN_POINT('',(0.115470053837925,-0.8,-0.2));
#9736=CARTESIAN_POINT('Origin',(-0.23094010767585,-0.5,-2.77555756156289E-17));
#9737=CARTESIAN_POINT('',(-0.23094010767585,-0.5,-2.82820063659975E-17));
#9738=CARTESIAN_POINT('',(-0.115470053837925,-0.5,-0.2));
#9739=CARTESIAN_POINT('',(-0.23094010767585,-0.8,-2.77555756156289E-17));
#9740=CARTESIAN_POINT('',(-0.23094010767585,-0.5,-2.82820063659975E-17));
#9741=CARTESIAN_POINT('',(-0.115470053837925,-0.8,-0.2));
#9742=CARTESIAN_POINT('Origin',(-0.115470053837925,-0.5,0.2));
#9743=CARTESIAN_POINT('',(-0.115470053837925,-0.5,0.2));
#9744=CARTESIAN_POINT('',(-0.23094010767585,-0.5,-2.82820063659975E-17));
#9745=CARTESIAN_POINT('',(-0.115470053837925,-0.8,0.2));
#9746=CARTESIAN_POINT('',(-0.115470053837925,-0.5,0.2));
#9747=CARTESIAN_POINT('',(-0.23094010767585,-0.8,-2.82820063659975E-17));
#9748=CARTESIAN_POINT('Origin',(0.115470053837925,-0.5,0.2));
#9749=CARTESIAN_POINT('',(0.115470053837925,-0.5,0.2));
#9750=CARTESIAN_POINT('',(-0.115470053837925,-0.5,0.2));
#9751=CARTESIAN_POINT('',(0.115470053837925,-0.8,0.2));
#9752=CARTESIAN_POINT('',(0.115470053837925,-0.5,0.2));
#9753=CARTESIAN_POINT('',(-0.115470053837925,-0.8,0.2));
#9754=CARTESIAN_POINT('Origin',(0.23094010767585,-0.5,0.));
#9755=CARTESIAN_POINT('',(0.115470053837925,-0.5,0.2));
#9756=CARTESIAN_POINT('',(0.115470053837925,-0.8,0.2));
#9757=CARTESIAN_POINT('Origin',(0.,-0.5,0.));
#9758=CARTESIAN_POINT('Origin',(0.,-0.8,0.));
#9759=CARTESIAN_POINT('Origin',(0.,-1.4,0.));
#9760=CARTESIAN_POINT('',(-0.24505,-1.4,3.00099698131059E-17));
#9761=CARTESIAN_POINT('Origin',(0.,-1.4,0.));
#9762=CARTESIAN_POINT('Origin',(0.375,0.5,0.));
#9763=CARTESIAN_POINT('',(-0.375,0.5,-4.59242549680257E-17));
#9764=CARTESIAN_POINT('Origin',(0.,0.5,0.));
#9765=CARTESIAN_POINT('Origin',(0.,0.475,0.));
#9766=CARTESIAN_POINT('',(-0.425,0.45,-5.20474889637625E-17));
#9767=CARTESIAN_POINT('Origin',(0.,0.45,0.));
#9768=CARTESIAN_POINT('',(-0.4,0.475,-4.89858719658941E-17));
#9769=CARTESIAN_POINT('Origin',(0.,0.24,0.));
#9770=CARTESIAN_POINT('',(-0.425,0.0299999999999998,-5.20474889637625E-17));
#9771=CARTESIAN_POINT('Origin',(0.,0.0299999999999998,0.));
#9772=CARTESIAN_POINT('',(-0.425,0.24,-5.20474889637625E-17));
#9773=CARTESIAN_POINT('Origin',(0.,0.0150000000000001,0.));
#9774=CARTESIAN_POINT('',(-0.395,4.85722573273506E-17,-4.83735485663204E-17));
#9775=CARTESIAN_POINT('Origin',(0.,0.,0.));
#9776=CARTESIAN_POINT('',(-0.41,0.0150000000000001,-5.02105187650415E-17));
#9777=CARTESIAN_POINT('Origin',(0.27,0.,0.));
#9778=CARTESIAN_POINT('',(-0.27,0.,-3.30654635769785E-17));
#9779=CARTESIAN_POINT('Origin',(0.,0.,0.));
#9780=CARTESIAN_POINT('Origin',(0.,-0.02,0.));
#9781=CARTESIAN_POINT('',(-0.24505,-0.0498999999999999,3.00099698131059E-17));
#9782=CARTESIAN_POINT('Origin',(0.,-0.0498999999999999,0.));
#9783=CARTESIAN_POINT('',(-0.26,-0.02,-3.18408167778312E-17));
#9784=CARTESIAN_POINT('Origin',(0.,-0.995,0.));
#9785=CARTESIAN_POINT('',(-0.24505,-0.995,-3.00099698131059E-17));
#9992=UNCERTAINTY_MEASURE_WITH_UNIT(LENGTH_MEASURE(0.001),#10020,
'DISTANCE_ACCURACY_VALUE',
'Maximum model space distance between geometric entities at asserted c
onnectivities');
#9995=UNCERTAINTY_MEASURE_WITH_UNIT(LENGTH_MEASURE(0.001),#10020,
'DISTANCE_ACCURACY_VALUE',
'Maximum model space distance between geometric entities at asserted c
onnectivities');
#10016=(
GEOMETRIC_REPRESENTATION_CONTEXT(3)
GLOBAL_UNCERTAINTY_ASSIGNED_CONTEXT((#9992))
GLOBAL_UNIT_ASSIGNED_CONTEXT((#10020,#10022,#10023))
REPRESENTATION_CONTEXT('','3D')
);
#10019=(
GEOMETRIC_REPRESENTATION_CONTEXT(3)
GLOBAL_UNCERTAINTY_ASSIGNED_CONTEXT((#9995))
GLOBAL_UNIT_ASSIGNED_CONTEXT((#10020,#10022,#10023))
REPRESENTATION_CONTEXT('','3D')
);
#10020=(
LENGTH_UNIT()
NAMED_UNIT(*)
SI_UNIT(.CENTI.,.METRE.)
);
#10022=(
NAMED_UNIT(*)
PLANE_ANGLE_UNIT()
SI_UNIT($,.RADIAN.)
);
#10023=(
NAMED_UNIT(*)
SI_UNIT($,.STERADIAN.)
SOLID_ANGLE_UNIT()
);
#10044=SHAPE_DEFINITION_REPRESENTATION(#10067,#10187);
#10067=PRODUCT_DEFINITION_SHAPE('',$,#10211);
#10187=SHAPE_REPRESENTATION('',(#6268),#10016);
#10190=PRODUCT_DEFINITION_CONTEXT('part definition',#10261,'design');
#10211=PRODUCT_DEFINITION('M5x14 Cap Screw','M5x14 Cap Screw',
#10234,#10190);
#10234=PRODUCT_DEFINITION_FORMATION('',$,#10283);
#10261=APPLICATION_CONTEXT(
'Core Data for Automotive Mechanical Design Process');
#10262=PRODUCT_CONTEXT('part definition',#10261,'mechanical');
#10283=PRODUCT('M5x14 Cap Screw','M5x14 Cap Screw',
'M5x14 Cap Screw',(#10262));
#10349=COLOUR_RGB('Black',0.12,0.14,0.17);
#10350=FILL_AREA_STYLE_COLOUR('',#10349);
#10351=FILL_AREA_STYLE('',(#10350));
#10352=SURFACE_STYLE_FILL_AREA(#10351);
#10353=SURFACE_SIDE_STYLE('',(#10352));
#10354=SURFACE_STYLE_USAGE(.BOTH.,#10353);
#10355=PRESENTATION_STYLE_ASSIGNMENT((#10354));
ENDSEC;
END-ISO-10303-21;
